ISO-10303-21;
HEADER;
/* Generated by software containing ST-Developer
 * from STEP Tools, Inc. (www.steptools.com) 
 */
/* OPTION: using custom renumber hook */

FILE_DESCRIPTION(
/* description */ ('STEP AP242 Edition 2', 'CAx-IF Rec.Pracs.---Representation and Presentation of Product Manufa
cturing Information (PMI)---4.0---2014-10-13', 'CAx-IF Rec.Pracs.---3D Tessellated Geometry---0.4---2014-09-14', '2;1', 'CAx-IF Rec.Pracs.---User Defined Attributes---1.5---2016-08-15'),
/* implementation_level */ '2;1');

FILE_NAME(
/* name */ 'screw_cover.step',
/* time_stamp */ '2026-10-08T12:15:07Z',
/* author */ (''),
/* organization */ (''),
/* preprocessor_version */ 'ST-DEVELOPER v20',
/* originating_system */ 'ONSHAPE BY PTC INC, 1.221',
/* authorisation */ '  ');

FILE_SCHEMA (('AP242_MANAGED_MODEL_BASED_3D_ENGINEERING_MIM_LF { 1 0 10303 442 3 1 4 }'));
ENDSEC;

DATA;
#60=COLOUR_RGB('', 0.66274510, 0.83137255, 0.94901961);
#219=SHAPE_REPRESENTATION_RELATIONSHIP('','',#13793,#246);
#246=ADVANCED_BREP_SHAPE_REPRESENTATION('',(#13737),#45483);
#807=CIRCLE('',#14766,0.001);
#808=CIRCLE('',#14767,0.001);
#809=CIRCLE('',#14771,0.001);
#810=CIRCLE('',#14773,0.001);
#811=CIRCLE('',#14774,0.001);
#812=CIRCLE('',#14778,0.001);
#813=CIRCLE('',#14780,0.001);
#814=CIRCLE('',#14781,0.001);
#815=CIRCLE('',#14785,0.001);
#816=CIRCLE('',#14787,0.00943317780363869);
#817=CIRCLE('',#14788,0.045);
#818=CIRCLE('',#14789,0.001);
#819=CIRCLE('',#14790,0.001);
#820=CIRCLE('',#14791,0.001);
#821=CIRCLE('',#14793,0.00943317780363869);
#822=CIRCLE('',#14794,0.045);
#1412=PLANE('',#14765);
#1413=PLANE('',#14768);
#1414=PLANE('',#14769);
#1415=PLANE('',#14772);
#1416=PLANE('',#14775);
#1417=PLANE('',#14776);
#1418=PLANE('',#14779);
#1419=PLANE('',#14782);
#1420=PLANE('',#14783);
#1421=PLANE('',#14786);
#1422=PLANE('',#14792);
#1717=CYLINDRICAL_SURFACE('',#14770,0.001);
#1718=CYLINDRICAL_SURFACE('',#14777,0.001);
#1719=CYLINDRICAL_SURFACE('',#14784,0.001);
#1720=CYLINDRICAL_SURFACE('',#14795,0.045);
#1721=CYLINDRICAL_SURFACE('',#14796,0.00943317780363869);
#1722=CYLINDRICAL_SURFACE('',#14797,0.001);
#1723=CYLINDRICAL_SURFACE('',#14798,0.001);
#1724=CYLINDRICAL_SURFACE('',#14799,0.001);
#4184=ORIENTED_EDGE('',*,*,#6739,.T.);
#4185=ORIENTED_EDGE('',*,*,#6740,.T.);
#4186=ORIENTED_EDGE('',*,*,#6741,.T.);
#4187=ORIENTED_EDGE('',*,*,#6742,.T.);
#4188=ORIENTED_EDGE('',*,*,#6742,.F.);
#4189=ORIENTED_EDGE('',*,*,#6743,.T.);
#4190=ORIENTED_EDGE('',*,*,#6744,.F.);
#4191=ORIENTED_EDGE('',*,*,#6745,.F.);
#4192=ORIENTED_EDGE('',*,*,#6740,.F.);
#4193=ORIENTED_EDGE('',*,*,#6746,.T.);
#4194=ORIENTED_EDGE('',*,*,#6747,.F.);
#4195=ORIENTED_EDGE('',*,*,#6748,.F.);
#4196=ORIENTED_EDGE('',*,*,#6739,.F.);
#4197=ORIENTED_EDGE('',*,*,#6745,.T.);
#4198=ORIENTED_EDGE('',*,*,#6749,.F.);
#4199=ORIENTED_EDGE('',*,*,#6746,.F.);
#4200=ORIENTED_EDGE('',*,*,#6750,.T.);
#4201=ORIENTED_EDGE('',*,*,#6751,.T.);
#4202=ORIENTED_EDGE('',*,*,#6752,.T.);
#4203=ORIENTED_EDGE('',*,*,#6753,.T.);
#4204=ORIENTED_EDGE('',*,*,#6753,.F.);
#4205=ORIENTED_EDGE('',*,*,#6754,.T.);
#4206=ORIENTED_EDGE('',*,*,#6755,.F.);
#4207=ORIENTED_EDGE('',*,*,#6756,.F.);
#4208=ORIENTED_EDGE('',*,*,#6751,.F.);
#4209=ORIENTED_EDGE('',*,*,#6757,.T.);
#4210=ORIENTED_EDGE('',*,*,#6758,.F.);
#4211=ORIENTED_EDGE('',*,*,#6759,.F.);
#4212=ORIENTED_EDGE('',*,*,#6750,.F.);
#4213=ORIENTED_EDGE('',*,*,#6756,.T.);
#4214=ORIENTED_EDGE('',*,*,#6760,.F.);
#4215=ORIENTED_EDGE('',*,*,#6757,.F.);
#4216=ORIENTED_EDGE('',*,*,#6761,.T.);
#4217=ORIENTED_EDGE('',*,*,#6762,.T.);
#4218=ORIENTED_EDGE('',*,*,#6763,.T.);
#4219=ORIENTED_EDGE('',*,*,#6764,.T.);
#4220=ORIENTED_EDGE('',*,*,#6764,.F.);
#4221=ORIENTED_EDGE('',*,*,#6765,.T.);
#4222=ORIENTED_EDGE('',*,*,#6766,.F.);
#4223=ORIENTED_EDGE('',*,*,#6767,.F.);
#4224=ORIENTED_EDGE('',*,*,#6762,.F.);
#4225=ORIENTED_EDGE('',*,*,#6768,.T.);
#4226=ORIENTED_EDGE('',*,*,#6769,.F.);
#4227=ORIENTED_EDGE('',*,*,#6770,.F.);
#4228=ORIENTED_EDGE('',*,*,#6761,.F.);
#4229=ORIENTED_EDGE('',*,*,#6767,.T.);
#4230=ORIENTED_EDGE('',*,*,#6771,.F.);
#4231=ORIENTED_EDGE('',*,*,#6768,.F.);
#4232=ORIENTED_EDGE('',*,*,#6772,.T.);
#4233=ORIENTED_EDGE('',*,*,#6773,.F.);
#4234=ORIENTED_EDGE('',*,*,#6769,.T.);
#4235=ORIENTED_EDGE('',*,*,#6771,.T.);
#4236=ORIENTED_EDGE('',*,*,#6766,.T.);
#4237=ORIENTED_EDGE('',*,*,#6774,.T.);
#4238=ORIENTED_EDGE('',*,*,#6758,.T.);
#4239=ORIENTED_EDGE('',*,*,#6760,.T.);
#4240=ORIENTED_EDGE('',*,*,#6755,.T.);
#4241=ORIENTED_EDGE('',*,*,#6775,.T.);
#4242=ORIENTED_EDGE('',*,*,#6747,.T.);
#4243=ORIENTED_EDGE('',*,*,#6749,.T.);
#4244=ORIENTED_EDGE('',*,*,#6744,.T.);
#4245=ORIENTED_EDGE('',*,*,#6776,.T.);
#4246=ORIENTED_EDGE('',*,*,#6777,.F.);
#4247=ORIENTED_EDGE('',*,*,#6778,.T.);
#4248=ORIENTED_EDGE('',*,*,#6773,.T.);
#4249=ORIENTED_EDGE('',*,*,#6778,.F.);
#4250=ORIENTED_EDGE('',*,*,#6772,.F.);
#4251=ORIENTED_EDGE('',*,*,#6777,.T.);
#4252=ORIENTED_EDGE('',*,*,#6763,.F.);
#4253=ORIENTED_EDGE('',*,*,#6770,.T.);
#4254=ORIENTED_EDGE('',*,*,#6774,.F.);
#4255=ORIENTED_EDGE('',*,*,#6765,.F.);
#4256=ORIENTED_EDGE('',*,*,#6752,.F.);
#4257=ORIENTED_EDGE('',*,*,#6759,.T.);
#4258=ORIENTED_EDGE('',*,*,#6775,.F.);
#4259=ORIENTED_EDGE('',*,*,#6754,.F.);
#4260=ORIENTED_EDGE('',*,*,#6741,.F.);
#4261=ORIENTED_EDGE('',*,*,#6748,.T.);
#4262=ORIENTED_EDGE('',*,*,#6776,.F.);
#4263=ORIENTED_EDGE('',*,*,#6743,.F.);
#6739=EDGE_CURVE('',#8258,#8259,#807,.T.);
#6740=EDGE_CURVE('',#8259,#8260,#9279,.T.);
#6741=EDGE_CURVE('',#8260,#8261,#808,.T.);
#6742=EDGE_CURVE('',#8261,#8258,#9280,.T.);
#6743=EDGE_CURVE('',#8261,#8262,#9281,.T.);
#6744=EDGE_CURVE('',#8263,#8262,#9282,.T.);
#6745=EDGE_CURVE('',#8258,#8263,#9283,.T.);
#6746=EDGE_CURVE('',#8259,#8264,#9284,.T.);
#6747=EDGE_CURVE('',#8265,#8264,#9285,.T.);
#6748=EDGE_CURVE('',#8260,#8265,#9286,.T.);
#6749=EDGE_CURVE('',#8264,#8263,#809,.T.);
#6750=EDGE_CURVE('',#8266,#8267,#810,.T.);
#6751=EDGE_CURVE('',#8267,#8268,#9287,.T.);
#6752=EDGE_CURVE('',#8268,#8269,#811,.T.);
#6753=EDGE_CURVE('',#8269,#8266,#9288,.T.);
#6754=EDGE_CURVE('',#8269,#8270,#9289,.T.);
#6755=EDGE_CURVE('',#8271,#8270,#9290,.T.);
#6756=EDGE_CURVE('',#8266,#8271,#9291,.T.);
#6757=EDGE_CURVE('',#8267,#8272,#9292,.T.);
#6758=EDGE_CURVE('',#8273,#8272,#9293,.T.);
#6759=EDGE_CURVE('',#8268,#8273,#9294,.T.);
#6760=EDGE_CURVE('',#8272,#8271,#812,.T.);
#6761=EDGE_CURVE('',#8274,#8275,#813,.T.);
#6762=EDGE_CURVE('',#8275,#8276,#9295,.T.);
#6763=EDGE_CURVE('',#8276,#8277,#814,.T.);
#6764=EDGE_CURVE('',#8277,#8274,#9296,.T.);
#6765=EDGE_CURVE('',#8277,#8278,#9297,.T.);
#6766=EDGE_CURVE('',#8279,#8278,#9298,.T.);
#6767=EDGE_CURVE('',#8274,#8279,#9299,.T.);
#6768=EDGE_CURVE('',#8275,#8280,#9300,.T.);
#6769=EDGE_CURVE('',#8281,#8280,#9301,.T.);
#6770=EDGE_CURVE('',#8276,#8281,#9302,.T.);
#6771=EDGE_CURVE('',#8280,#8279,#815,.T.);
#6772=EDGE_CURVE('',#8282,#8282,#816,.T.);
#6773=EDGE_CURVE('',#8283,#8283,#817,.T.);
#6774=EDGE_CURVE('',#8278,#8281,#818,.T.);
#6775=EDGE_CURVE('',#8270,#8273,#819,.T.);
#6776=EDGE_CURVE('',#8262,#8265,#820,.T.);
#6777=EDGE_CURVE('',#8284,#8284,#821,.T.);
#6778=EDGE_CURVE('',#8285,#8285,#822,.T.);
#8258=VERTEX_POINT('',#35187);
#8259=VERTEX_POINT('',#35188);
#8260=VERTEX_POINT('',#35190);
#8261=VERTEX_POINT('',#35192);
#8262=VERTEX_POINT('',#35196);
#8263=VERTEX_POINT('',#35198);
#8264=VERTEX_POINT('',#35202);
#8265=VERTEX_POINT('',#35204);
#8266=VERTEX_POINT('',#35210);
#8267=VERTEX_POINT('',#35211);
#8268=VERTEX_POINT('',#35213);
#8269=VERTEX_POINT('',#35215);
#8270=VERTEX_POINT('',#35219);
#8271=VERTEX_POINT('',#35221);
#8272=VERTEX_POINT('',#35225);
#8273=VERTEX_POINT('',#35227);
#8274=VERTEX_POINT('',#35233);
#8275=VERTEX_POINT('',#35234);
#8276=VERTEX_POINT('',#35236);
#8277=VERTEX_POINT('',#35238);
#8278=VERTEX_POINT('',#35242);
#8279=VERTEX_POINT('',#35244);
#8280=VERTEX_POINT('',#35248);
#8281=VERTEX_POINT('',#35250);
#8282=VERTEX_POINT('',#35256);
#8283=VERTEX_POINT('',#35258);
#8284=VERTEX_POINT('',#35264);
#8285=VERTEX_POINT('',#35266);
#9279=LINE('',#35189,#10107);
#9280=LINE('',#35193,#10108);
#9281=LINE('',#35195,#10109);
#9282=LINE('',#35197,#10110);
#9283=LINE('',#35199,#10111);
#9284=LINE('',#35201,#10112);
#9285=LINE('',#35203,#10113);
#9286=LINE('',#35205,#10114);
#9287=LINE('',#35212,#10115);
#9288=LINE('',#35216,#10116);
#9289=LINE('',#35218,#10117);
#9290=LINE('',#35220,#10118);
#9291=LINE('',#35222,#10119);
#9292=LINE('',#35224,#10120);
#9293=LINE('',#35226,#10121);
#9294=LINE('',#35228,#10122);
#9295=LINE('',#35235,#10123);
#9296=LINE('',#35239,#10124);
#9297=LINE('',#35241,#10125);
#9298=LINE('',#35243,#10126);
#9299=LINE('',#35245,#10127);
#9300=LINE('',#35247,#10128);
#9301=LINE('',#35249,#10129);
#9302=LINE('',#35251,#10130);
#10107=VECTOR('',#17731,1.);
#10108=VECTOR('',#17734,1.);
#10109=VECTOR('',#17737,1.);
#10110=VECTOR('',#17738,1.);
#10111=VECTOR('',#17739,1.);
#10112=VECTOR('',#17742,1.);
#10113=VECTOR('',#17743,1.);
#10114=VECTOR('',#17744,1.);
#10115=VECTOR('',#17753,1.);
#10116=VECTOR('',#17756,1.);
#10117=VECTOR('',#17759,1.);
#10118=VECTOR('',#17760,1.);
#10119=VECTOR('',#17761,1.);
#10120=VECTOR('',#17764,1.);
#10121=VECTOR('',#17765,1.);
#10122=VECTOR('',#17766,1.);
#10123=VECTOR('',#17775,1.);
#10124=VECTOR('',#17778,1.);
#10125=VECTOR('',#17781,1.);
#10126=VECTOR('',#17782,1.);
#10127=VECTOR('',#17783,1.);
#10128=VECTOR('',#17786,1.);
#10129=VECTOR('',#17787,1.);
#10130=VECTOR('',#17788,1.);
#11150=EDGE_LOOP('',(#4184,#4185,#4186,#4187));
#11151=EDGE_LOOP('',(#4188,#4189,#4190,#4191));
#11152=EDGE_LOOP('',(#4192,#4193,#4194,#4195));
#11153=EDGE_LOOP('',(#4196,#4197,#4198,#4199));
#11154=EDGE_LOOP('',(#4200,#4201,#4202,#4203));
#11155=EDGE_LOOP('',(#4204,#4205,#4206,#4207));
#11156=EDGE_LOOP('',(#4208,#4209,#4210,#4211));
#11157=EDGE_LOOP('',(#4212,#4213,#4214,#4215));
#11158=EDGE_LOOP('',(#4216,#4217,#4218,#4219));
#11159=EDGE_LOOP('',(#4220,#4221,#4222,#4223));
#11160=EDGE_LOOP('',(#4224,#4225,#4226,#4227));
#11161=EDGE_LOOP('',(#4228,#4229,#4230,#4231));
#11162=EDGE_LOOP('',(#4232));
#11163=EDGE_LOOP('',(#4233));
#11164=EDGE_LOOP('',(#4234,#4235,#4236,#4237));
#11165=EDGE_LOOP('',(#4238,#4239,#4240,#4241));
#11166=EDGE_LOOP('',(#4242,#4243,#4244,#4245));
#11167=EDGE_LOOP('',(#4246));
#11168=EDGE_LOOP('',(#4247));
#11169=EDGE_LOOP('',(#4248));
#11170=EDGE_LOOP('',(#4249));
#11171=EDGE_LOOP('',(#4250));
#11172=EDGE_LOOP('',(#4251));
#11173=EDGE_LOOP('',(#4252,#4253,#4254,#4255));
#11174=EDGE_LOOP('',(#4256,#4257,#4258,#4259));
#11175=EDGE_LOOP('',(#4260,#4261,#4262,#4263));
#12269=FACE_BOUND('',#11150,.T.);
#12270=FACE_BOUND('',#11151,.T.);
#12271=FACE_BOUND('',#11152,.T.);
#12272=FACE_BOUND('',#11153,.T.);
#12273=FACE_BOUND('',#11154,.T.);
#12274=FACE_BOUND('',#11155,.T.);
#12275=FACE_BOUND('',#11156,.T.);
#12276=FACE_BOUND('',#11157,.T.);
#12277=FACE_BOUND('',#11158,.T.);
#12278=FACE_BOUND('',#11159,.T.);
#12279=FACE_BOUND('',#11160,.T.);
#12280=FACE_BOUND('',#11161,.T.);
#12281=FACE_BOUND('',#11162,.T.);
#12282=FACE_BOUND('',#11163,.T.);
#12283=FACE_BOUND('',#11164,.T.);
#12284=FACE_BOUND('',#11165,.T.);
#12285=FACE_BOUND('',#11166,.T.);
#12286=FACE_BOUND('',#11167,.T.);
#12287=FACE_BOUND('',#11168,.T.);
#12288=FACE_BOUND('',#11169,.T.);
#12289=FACE_BOUND('',#11170,.T.);
#12290=FACE_BOUND('',#11171,.T.);
#12291=FACE_BOUND('',#11172,.T.);
#12292=FACE_BOUND('',#11173,.T.);
#12293=FACE_BOUND('',#11174,.T.);
#12294=FACE_BOUND('',#11175,.T.);
#13213=ADVANCED_FACE('',(#12269),#1412,.F.);
#13214=ADVANCED_FACE('',(#12270),#1413,.T.);
#13215=ADVANCED_FACE('',(#12271),#1414,.T.);
#13216=ADVANCED_FACE('',(#12272),#1717,.T.);
#13217=ADVANCED_FACE('',(#12273),#1415,.F.);
#13218=ADVANCED_FACE('',(#12274),#1416,.T.);
#13219=ADVANCED_FACE('',(#12275),#1417,.T.);
#13220=ADVANCED_FACE('',(#12276),#1718,.T.);
#13221=ADVANCED_FACE('',(#12277),#1418,.F.);
#13222=ADVANCED_FACE('',(#12278),#1419,.T.);
#13223=ADVANCED_FACE('',(#12279),#1420,.T.);
#13224=ADVANCED_FACE('',(#12280),#1719,.T.);
#13225=ADVANCED_FACE('',(#12281,#12282,#12283,#12284,#12285),#1421,.F.);
#13226=ADVANCED_FACE('',(#12286,#12287),#1422,.T.);
#13227=ADVANCED_FACE('',(#12288,#12289),#1720,.T.);
#13228=ADVANCED_FACE('',(#12290,#12291),#1721,.F.);
#13229=ADVANCED_FACE('',(#12292),#1722,.T.);
#13230=ADVANCED_FACE('',(#12293),#1723,.T.);
#13231=ADVANCED_FACE('',(#12294),#1724,.T.);
#13520=CLOSED_SHELL('',(#13213,#13214,#13215,#13216,#13217,#13218,#13219,
#13220,#13221,#13222,#13223,#13224,#13225,#13226,#13227,#13228,#13229,#13230,
#13231));
#13547=STYLED_ITEM('',(#13574),#13737);
#13574=PRESENTATION_STYLE_ASSIGNMENT((#13601));
#13601=SURFACE_STYLE_USAGE(.BOTH.,#13628);
#13628=SURFACE_SIDE_STYLE('',(#13655));
#13655=SURFACE_STYLE_FILL_AREA(#13682);
#13682=FILL_AREA_STYLE('',(#13709));
#13709=FILL_AREA_STYLE_COLOUR('',#60);
#13737=MANIFOLD_SOLID_BREP('screw_cover',#13520);
#13765=SHAPE_DEFINITION_REPRESENTATION(#45565,#13793);
#13793=SHAPE_REPRESENTATION('screw_cover',(#13802),#45483);
#13802=AXIS2_PLACEMENT_3D('',#19109,#15295,#15296);
#14765=AXIS2_PLACEMENT_3D('',#35185,#17727,#17728);
#14766=AXIS2_PLACEMENT_3D('',#35186,#17729,#17730);
#14767=AXIS2_PLACEMENT_3D('',#35191,#17732,#17733);
#14768=AXIS2_PLACEMENT_3D('',#35194,#17735,#17736);
#14769=AXIS2_PLACEMENT_3D('',#35200,#17740,#17741);
#14770=AXIS2_PLACEMENT_3D('',#35206,#17745,#17746);
#14771=AXIS2_PLACEMENT_3D('',#35207,#17747,#17748);
#14772=AXIS2_PLACEMENT_3D('',#35208,#17749,#17750);
#14773=AXIS2_PLACEMENT_3D('',#35209,#17751,#17752);
#14774=AXIS2_PLACEMENT_3D('',#35214,#17754,#17755);
#14775=AXIS2_PLACEMENT_3D('',#35217,#17757,#17758);
#14776=AXIS2_PLACEMENT_3D('',#35223,#17762,#17763);
#14777=AXIS2_PLACEMENT_3D('',#35229,#17767,#17768);
#14778=AXIS2_PLACEMENT_3D('',#35230,#17769,#17770);
#14779=AXIS2_PLACEMENT_3D('',#35231,#17771,#17772);
#14780=AXIS2_PLACEMENT_3D('',#35232,#17773,#17774);
#14781=AXIS2_PLACEMENT_3D('',#35237,#17776,#17777);
#14782=AXIS2_PLACEMENT_3D('',#35240,#17779,#17780);
#14783=AXIS2_PLACEMENT_3D('',#35246,#17784,#17785);
#14784=AXIS2_PLACEMENT_3D('',#35252,#17789,#17790);
#14785=AXIS2_PLACEMENT_3D('',#35253,#17791,#17792);
#14786=AXIS2_PLACEMENT_3D('',#35254,#17793,#17794);
#14787=AXIS2_PLACEMENT_3D('',#35255,#17795,#17796);
#14788=AXIS2_PLACEMENT_3D('',#35257,#17797,#17798);
#14789=AXIS2_PLACEMENT_3D('',#35259,#17799,#17800);
#14790=AXIS2_PLACEMENT_3D('',#35260,#17801,#17802);
#14791=AXIS2_PLACEMENT_3D('',#35261,#17803,#17804);
#14792=AXIS2_PLACEMENT_3D('',#35262,#17805,#17806);
#14793=AXIS2_PLACEMENT_3D('',#35263,#17807,#17808);
#14794=AXIS2_PLACEMENT_3D('',#35265,#17809,#17810);
#14795=AXIS2_PLACEMENT_3D('',#35267,#17811,#17812);
#14796=AXIS2_PLACEMENT_3D('',#35268,#17813,#17814);
#14797=AXIS2_PLACEMENT_3D('',#35269,#17815,#17816);
#14798=AXIS2_PLACEMENT_3D('',#35270,#17817,#17818);
#14799=AXIS2_PLACEMENT_3D('',#35271,#17819,#17820);
#15295=DIRECTION('',(0.,0.,1.));
#15296=DIRECTION('',(1.,0.,0.));
#17727=DIRECTION('',(0.,0.,1.));
#17728=DIRECTION('',(1.,0.,0.));
#17729=DIRECTION('',(0.,0.,-1.));
#17730=DIRECTION('',(-0.499999999999991,-0.866025403784444,0.));
#17731=DIRECTION('',(0.500000000000011,-0.866025403784433,0.));
#17732=DIRECTION('',(0.,0.,-1.));
#17733=DIRECTION('',(-0.499999999999993,-0.866025403784443,0.));
#17734=DIRECTION('',(-0.50000000000001,0.866025403784433,0.));
#17735=DIRECTION('',(-0.866025403784433,-0.50000000000001,0.));
#17736=DIRECTION('',(0.50000000000001,-0.866025403784433,0.));
#17737=DIRECTION('',(0.,0.,1.));
#17738=DIRECTION('',(0.50000000000001,-0.866025403784433,0.));
#17739=DIRECTION('',(0.,0.,1.));
#17740=DIRECTION('',(0.866025403784433,0.500000000000011,0.));
#17741=DIRECTION('',(-0.500000000000011,0.866025403784433,0.));
#17742=DIRECTION('',(0.,0.,1.));
#17743=DIRECTION('',(-0.500000000000011,0.866025403784433,0.));
#17744=DIRECTION('',(0.,0.,1.));
#17745=DIRECTION('',(0.,0.,1.));
#17746=DIRECTION('',(-0.499999999999993,-0.866025403784443,0.));
#17747=DIRECTION('',(0.,0.,1.));
#17748=DIRECTION('',(-0.499999999999993,-0.866025403784443,0.));
#17749=DIRECTION('',(0.,0.,1.));
#17750=DIRECTION('',(1.,0.,0.));
#17751=DIRECTION('',(0.,0.,-1.));
#17752=DIRECTION('',(-0.5,0.866025403784436,0.));
#17753=DIRECTION('',(-1.,-7.66053886991358E-15,0.));
#17754=DIRECTION('',(0.,0.,-1.));
#17755=DIRECTION('',(-0.5,0.866025403784437,0.));
#17756=DIRECTION('',(1.,7.27196081129478E-15,0.));
#17757=DIRECTION('',(0.,1.,0.));
#17758=DIRECTION('',(-1.,0.,0.));
#17759=DIRECTION('',(0.,0.,1.));
#17760=DIRECTION('',(-1.,-7.27196081129478E-15,0.));
#17761=DIRECTION('',(0.,0.,1.));
#17762=DIRECTION('',(0.,-1.,0.));
#17763=DIRECTION('',(1.,0.,0.));
#17764=DIRECTION('',(0.,0.,1.));
#17765=DIRECTION('',(1.,7.66053886991358E-15,0.));
#17766=DIRECTION('',(0.,0.,1.));
#17767=DIRECTION('',(0.,0.,1.));
#17768=DIRECTION('',(-0.5,0.866025403784436,0.));
#17769=DIRECTION('',(0.,0.,1.));
#17770=DIRECTION('',(-0.5,0.866025403784436,0.));
#17771=DIRECTION('',(0.,0.,1.));
#17772=DIRECTION('',(1.,0.,0.));
#17773=DIRECTION('',(0.,0.,-1.));
#17774=DIRECTION('',(1.,3.46944695195361E-15,0.));
#17775=DIRECTION('',(0.5,0.86602540378444,0.));
#17776=DIRECTION('',(0.,0.,-1.));
#17777=DIRECTION('',(1.,0.,0.));
#17778=DIRECTION('',(-0.5,-0.86602540378444,0.));
#17779=DIRECTION('',(0.86602540378444,-0.5,0.));
#17780=DIRECTION('',(0.5,0.86602540378444,0.));
#17781=DIRECTION('',(0.,0.,1.));
#17782=DIRECTION('',(0.5,0.86602540378444,0.));
#17783=DIRECTION('',(0.,0.,1.));
#17784=DIRECTION('',(-0.86602540378444,0.5,0.));
#17785=DIRECTION('',(-0.5,-0.86602540378444,0.));
#17786=DIRECTION('',(0.,0.,1.));
#17787=DIRECTION('',(-0.5,-0.86602540378444,0.));
#17788=DIRECTION('',(0.,0.,1.));
#17789=DIRECTION('',(0.,0.,1.));
#17790=DIRECTION('',(1.,0.,0.));
#17791=DIRECTION('',(0.,0.,1.));
#17792=DIRECTION('',(1.,0.,0.));
#17793=DIRECTION('',(0.,0.,1.));
#17794=DIRECTION('',(1.,0.,0.));
#17795=DIRECTION('',(0.,0.,1.));
#17796=DIRECTION('',(1.,0.,0.));
#17797=DIRECTION('',(0.,0.,1.));
#17798=DIRECTION('',(1.,0.,0.));
#17799=DIRECTION('',(0.,0.,1.));
#17800=DIRECTION('',(1.,0.,0.));
#17801=DIRECTION('',(0.,0.,1.));
#17802=DIRECTION('',(-0.5,0.866025403784436,0.));
#17803=DIRECTION('',(0.,0.,1.));
#17804=DIRECTION('',(-0.499999999999993,-0.866025403784443,0.));
#17805=DIRECTION('',(0.,0.,1.));
#17806=DIRECTION('',(1.,0.,0.));
#17807=DIRECTION('',(0.,0.,1.));
#17808=DIRECTION('',(1.,0.,0.));
#17809=DIRECTION('',(0.,0.,1.));
#17810=DIRECTION('',(1.,0.,0.));
#17811=DIRECTION('',(0.,0.,-1.));
#17812=DIRECTION('',(-1.,0.,0.));
#17813=DIRECTION('',(0.,0.,-1.));
#17814=DIRECTION('',(-1.,0.,0.));
#17815=DIRECTION('',(0.,0.,1.));
#17816=DIRECTION('',(1.,0.,0.));
#17817=DIRECTION('',(0.,0.,1.));
#17818=DIRECTION('',(-0.5,0.866025403784436,0.));
#17819=DIRECTION('',(0.,0.,1.));
#17820=DIRECTION('',(-0.499999999999993,-0.866025403784443,0.));
#19109=CARTESIAN_POINT('',(0.,0.,0.));
#35185=CARTESIAN_POINT('',(0.,0.,0.1));
#35186=CARTESIAN_POINT('',(0.0311589653438084,0.0220310889132459,0.1));
#35187=CARTESIAN_POINT('',(0.030292939940024,0.0215310889132459,0.1));
#35188=CARTESIAN_POINT('',(0.0320249907475929,0.0225310889132459,0.1));
#35189=CARTESIAN_POINT('',(0.0320249907475929,0.0225310889132459,0.1));
#35190=CARTESIAN_POINT('',(0.0355249907475929,0.0164689110867549,0.1));
#35191=CARTESIAN_POINT('',(0.0346589653438085,0.0159689110867548,0.1));
#35192=CARTESIAN_POINT('',(0.033792939940024,0.0154689110867548,0.1));
#35193=CARTESIAN_POINT('',(0.030292939940024,0.0215310889132459,0.1));
#35194=CARTESIAN_POINT('',(0.030292939940024,0.0215310889132459,0.0902404553740472));
#35195=CARTESIAN_POINT('',(0.033792939940024,0.0154689110867548,0.0902404553740472));
#35196=CARTESIAN_POINT('',(0.033792939940024,0.0154689110867548,0.103));
#35197=CARTESIAN_POINT('',(0.030292939940024,0.0215310889132459,0.103));
#35198=CARTESIAN_POINT('',(0.030292939940024,0.0215310889132459,0.103));
#35199=CARTESIAN_POINT('',(0.030292939940024,0.0215310889132459,0.0902404553740472));
#35200=CARTESIAN_POINT('',(0.0320249907475929,0.0225310889132459,0.0902404553740472));
#35201=CARTESIAN_POINT('',(0.0320249907475929,0.0225310889132459,0.0902404553740472));
#35202=CARTESIAN_POINT('',(0.0320249907475929,0.0225310889132459,0.103));
#35203=CARTESIAN_POINT('',(0.0320249907475929,0.0225310889132459,0.103));
#35204=CARTESIAN_POINT('',(0.0355249907475929,0.0164689110867549,0.103));
#35205=CARTESIAN_POINT('',(0.0355249907475929,0.0164689110867549,0.0902404553740472));
#35206=CARTESIAN_POINT('',(0.0311589653438084,0.0220310889132459,0.0902404553740472));
#35207=CARTESIAN_POINT('',(0.0311589653438084,0.0220310889132459,0.103));
#35208=CARTESIAN_POINT('',(0.,0.,0.1));
#35209=CARTESIAN_POINT('',(0.00350000000000028,-0.038,0.1));
#35210=CARTESIAN_POINT('',(0.00350000000000027,-0.037,0.1));
#35211=CARTESIAN_POINT('',(0.00350000000000029,-0.039,0.1));
#35212=CARTESIAN_POINT('',(0.00350000000000029,-0.039,0.1));
#35213=CARTESIAN_POINT('',(-0.00349999999999972,-0.039,0.1));
#35214=CARTESIAN_POINT('',(-0.00349999999999973,-0.038,0.1));
#35215=CARTESIAN_POINT('',(-0.00349999999999974,-0.037,0.1));
#35216=CARTESIAN_POINT('',(0.00350000000000028,-0.037,0.1));
#35217=CARTESIAN_POINT('',(0.00350000000000028,-0.037,0.0902404553740472));
#35218=CARTESIAN_POINT('',(-0.00349999999999974,-0.037,0.0902404553740472));
#35219=CARTESIAN_POINT('',(-0.00349999999999974,-0.037,0.103));
#35220=CARTESIAN_POINT('',(0.00350000000000028,-0.037,0.103));
#35221=CARTESIAN_POINT('',(0.00350000000000027,-0.037,0.103));
#35222=CARTESIAN_POINT('',(0.00350000000000028,-0.037,0.0902404553740472));
#35223=CARTESIAN_POINT('',(0.00350000000000029,-0.039,0.0902404553740472));
#35224=CARTESIAN_POINT('',(0.00350000000000029,-0.039,0.0902404553740472));
#35225=CARTESIAN_POINT('',(0.00350000000000029,-0.039,0.103));
#35226=CARTESIAN_POINT('',(0.00350000000000029,-0.039,0.103));
#35227=CARTESIAN_POINT('',(-0.00349999999999972,-0.039,0.103));
#35228=CARTESIAN_POINT('',(-0.00349999999999972,-0.039,0.0902404553740472));
#35229=CARTESIAN_POINT('',(0.00350000000000028,-0.038,0.0902404553740472));
#35230=CARTESIAN_POINT('',(0.00350000000000028,-0.038,0.103));
#35231=CARTESIAN_POINT('',(0.,0.,0.1));
#35232=CARTESIAN_POINT('',(-0.0346589653438087,0.0159689110867543,0.1));
#35233=CARTESIAN_POINT('',(-0.0337929399400243,0.0154689110867544,0.1));
#35234=CARTESIAN_POINT('',(-0.0355249907475932,0.0164689110867543,0.1));
#35235=CARTESIAN_POINT('',(-0.0355249907475932,0.0164689110867543,0.1));
#35236=CARTESIAN_POINT('',(-0.0320249907475932,0.0225310889132454,0.1));
#35237=CARTESIAN_POINT('',(-0.0311589653438087,0.0220310889132454,0.1));
#35238=CARTESIAN_POINT('',(-0.0302929399400243,0.0215310889132454,0.1));
#35239=CARTESIAN_POINT('',(-0.0337929399400243,0.0154689110867544,0.1));
#35240=CARTESIAN_POINT('',(-0.0337929399400243,0.0154689110867544,0.0902404553740472));
#35241=CARTESIAN_POINT('',(-0.0302929399400243,0.0215310889132454,0.0902404553740472));
#35242=CARTESIAN_POINT('',(-0.0302929399400243,0.0215310889132454,0.103));
#35243=CARTESIAN_POINT('',(-0.0337929399400243,0.0154689110867544,0.103));
#35244=CARTESIAN_POINT('',(-0.0337929399400243,0.0154689110867544,0.103));
#35245=CARTESIAN_POINT('',(-0.0337929399400243,0.0154689110867544,0.0902404553740472));
#35246=CARTESIAN_POINT('',(-0.0355249907475932,0.0164689110867543,0.0902404553740472));
#35247=CARTESIAN_POINT('',(-0.0355249907475932,0.0164689110867543,0.0902404553740472));
#35248=CARTESIAN_POINT('',(-0.0355249907475932,0.0164689110867543,0.103));
#35249=CARTESIAN_POINT('',(-0.0355249907475932,0.0164689110867543,0.103));
#35250=CARTESIAN_POINT('',(-0.0320249907475932,0.0225310889132454,0.103));
#35251=CARTESIAN_POINT('',(-0.0320249907475932,0.0225310889132454,0.0902404553740472));
#35252=CARTESIAN_POINT('',(-0.0346589653438087,0.0159689110867543,0.0902404553740472));
#35253=CARTESIAN_POINT('',(-0.0346589653438087,0.0159689110867543,0.103));
#35254=CARTESIAN_POINT('',(0.,0.,0.103));
#35255=CARTESIAN_POINT('',(0.,0.,0.103));
#35256=CARTESIAN_POINT('',(0.00943317780363869,0.,0.103));
#35257=CARTESIAN_POINT('',(0.,0.,0.103));
#35258=CARTESIAN_POINT('',(0.045,0.,0.103));
#35259=CARTESIAN_POINT('',(-0.0311589653438087,0.0220310889132454,0.103));
#35260=CARTESIAN_POINT('',(-0.00349999999999973,-0.038,0.103));
#35261=CARTESIAN_POINT('',(0.0346589653438085,0.0159689110867548,0.103));
#35262=CARTESIAN_POINT('',(0.,0.,0.104));
#35263=CARTESIAN_POINT('',(0.,0.,0.104));
#35264=CARTESIAN_POINT('',(0.00943317780363869,0.,0.104));
#35265=CARTESIAN_POINT('',(0.,0.,0.104));
#35266=CARTESIAN_POINT('',(0.045,0.,0.104));
#35267=CARTESIAN_POINT('',(0.,0.,0.104));
#35268=CARTESIAN_POINT('',(0.,0.,0.104));
#35269=CARTESIAN_POINT('',(-0.0311589653438087,0.0220310889132454,0.0902404553740472));
#35270=CARTESIAN_POINT('',(-0.00349999999999973,-0.038,0.0902404553740472));
#35271=CARTESIAN_POINT('',(0.0346589653438085,0.0159689110867548,0.0902404553740472));
#45463=MECHANICAL_DESIGN_GEOMETRIC_PRESENTATION_REPRESENTATION('',(#13547),#45464);
#45464=(
GEOMETRIC_REPRESENTATION_CONTEXT(3)
GLOBAL_UNCERTAINTY_ASSIGNED_CONTEXT((#45492))
GLOBAL_UNIT_ASSIGNED_CONTEXT((#45522,#45521,#45520))
REPRESENTATION_CONTEXT('MAS-690','TOP_LEVEL_ASSEMBLY_PART')
);
#45483=(
GEOMETRIC_REPRESENTATION_CONTEXT(3)
GLOBAL_UNCERTAINTY_ASSIGNED_CONTEXT((#45511))
GLOBAL_UNIT_ASSIGNED_CONTEXT((#45522,#45521,#45520))
REPRESENTATION_CONTEXT('screw_cover','COMPONENT_PART')
);
#45492=UNCERTAINTY_MEASURE_WITH_UNIT(LENGTH_MEASURE(1.E-8),#45522,
'DISTANCE_ACCURACY_VALUE','Maximum Tolerance applied to model');
#45511=UNCERTAINTY_MEASURE_WITH_UNIT(LENGTH_MEASURE(1.E-6),#45522,
'DISTANCE_ACCURACY_VALUE','Maximum Tolerance applied to model');
#45520=(
NAMED_UNIT(*)
SI_UNIT($,.STERADIAN.)
SOLID_ANGLE_UNIT()
);
#45521=(
NAMED_UNIT(*)
PLANE_ANGLE_UNIT()
SI_UNIT($,.RADIAN.)
);
#45522=(
LENGTH_UNIT()
NAMED_UNIT(*)
SI_UNIT($,.METRE.)
);
#45565=PRODUCT_DEFINITION_SHAPE('','',#45604);
#45604=PRODUCT_DEFINITION('','',#45660,#45632);
#45632=PRODUCT_DEFINITION_CONTEXT('',#45782,'design');
#45660=PRODUCT_DEFINITION_FORMATION_WITH_SPECIFIED_SOURCE('','',#45716,
 .NOT_KNOWN.);
#45716=PRODUCT('screw_cover','screw_cover','screw_cover',(#45772));
#45772=PRODUCT_CONTEXT('',#45782,'mechanical');
#45782=APPLICATION_CONTEXT('managed model based 3d engineering');
ENDSEC;
END-ISO-10303-21;
